ISO-10303-21;
HEADER;
/* Generated by software containing ST-Developer
 * from STEP Tools, Inc. (www.steptools.com) 
 */

FILE_DESCRIPTION(
/* description */ ('Belt tension measurement rig'),
/* implementation_level */ '2;1');

FILE_NAME(
/* name */ 'Screw bushing.step',
/* time_stamp */ '2026-10-28T03:24:44-07:00',
/* author */ (''),
/* organization */ (''),
/* preprocessor_version */ 'ST-DEVELOPER v20.2',
/* originating_system */ 'Autodesk Translation Framework v15.17.0.0',
/* authorisation */ '');

FILE_SCHEMA (('AUTOMOTIVE_DESIGN { 1 0 10303 214 3 1 1 }'));
ENDSEC;

DATA;
#10=MECHANICAL_DESIGN_GEOMETRIC_PRESENTATION_REPRESENTATION('',(#700),#23587);
#590=SHAPE_REPRESENTATION_RELATIONSHIP('SRR','None',#23835,#645);
#645=ADVANCED_BREP_SHAPE_REPRESENTATION('',(#770),#23533);
#700=STYLED_ITEM('',(#24218),#770);
#770=MANIFOLD_SOLID_BREP('Body1',#12205);
#877=FACE_BOUND('',#2215,.T.);
#878=FACE_BOUND('',#2217,.T.);
#1095=PLANE('',#13101);
#1096=PLANE('',#13102);
#1460=FACE_OUTER_BOUND('',#2212,.T.);
#1461=FACE_OUTER_BOUND('',#2213,.T.);
#1462=FACE_OUTER_BOUND('',#2214,.T.);
#1463=FACE_OUTER_BOUND('',#2216,.T.);
#2212=EDGE_LOOP('',(#8382,#8383,#8384,#8385));
#2213=EDGE_LOOP('',(#8386,#8387,#8388,#8389));
#2214=EDGE_LOOP('',(#8390));
#2215=EDGE_LOOP('',(#8391));
#2216=EDGE_LOOP('',(#8392));
#2217=EDGE_LOOP('',(#8393));
#3090=LINE('',#19043,#3841);
#3091=LINE('',#19049,#3842);
#3841=VECTOR('',#15081,0.605);
#3842=VECTOR('',#15088,0.8);
#4570=CIRCLE('',#13096,0.605);
#4571=CIRCLE('',#13097,0.605);
#4572=CIRCLE('',#13099,0.8);
#4573=CIRCLE('',#13100,0.8);
#5386=VERTEX_POINT('',#19040);
#5387=VERTEX_POINT('',#19042);
#5388=VERTEX_POINT('',#19046);
#5389=VERTEX_POINT('',#19048);
#6550=EDGE_CURVE('',#5386,#5386,#4570,.T.);
#6551=EDGE_CURVE('',#5386,#5387,#3090,.T.);
#6552=EDGE_CURVE('',#5387,#5387,#4571,.T.);
#6553=EDGE_CURVE('',#5388,#5388,#4572,.T.);
#6554=EDGE_CURVE('',#5388,#5389,#3091,.T.);
#6555=EDGE_CURVE('',#5389,#5389,#4573,.T.);
#8382=ORIENTED_EDGE('',*,*,#6550,.F.);
#8383=ORIENTED_EDGE('',*,*,#6551,.T.);
#8384=ORIENTED_EDGE('',*,*,#6552,.T.);
#8385=ORIENTED_EDGE('',*,*,#6551,.F.);
#8386=ORIENTED_EDGE('',*,*,#6553,.F.);
#8387=ORIENTED_EDGE('',*,*,#6554,.T.);
#8388=ORIENTED_EDGE('',*,*,#6555,.T.);
#8389=ORIENTED_EDGE('',*,*,#6554,.F.);
#8390=ORIENTED_EDGE('',*,*,#6553,.T.);
#8391=ORIENTED_EDGE('',*,*,#6550,.T.);
#8392=ORIENTED_EDGE('',*,*,#6555,.F.);
#8393=ORIENTED_EDGE('',*,*,#6552,.F.);
#11208=CYLINDRICAL_SURFACE('',#13095,0.605);
#11209=CYLINDRICAL_SURFACE('',#13098,0.8);
#11601=ADVANCED_FACE('',(#1460),#11208,.F.);
#11602=ADVANCED_FACE('',(#1461),#11209,.T.);
#11603=ADVANCED_FACE('',(#1462,#877),#1095,.T.);
#11604=ADVANCED_FACE('',(#1463,#878),#1096,.F.);
#12205=CLOSED_SHELL('',(#11601,#11602,#11603,#11604));
#13094=AXIS2_PLACEMENT_3D('',#19038,#15075,#15076);
#13095=AXIS2_PLACEMENT_3D('',#19039,#15077,#15078);
#13096=AXIS2_PLACEMENT_3D('',#19041,#15079,#15080);
#13097=AXIS2_PLACEMENT_3D('',#19044,#15082,#15083);
#13098=AXIS2_PLACEMENT_3D('',#19045,#15084,#15085);
#13099=AXIS2_PLACEMENT_3D('',#19047,#15086,#15087);
#13100=AXIS2_PLACEMENT_3D('',#19050,#15089,#15090);
#13101=AXIS2_PLACEMENT_3D('',#19051,#15091,#15092);
#13102=AXIS2_PLACEMENT_3D('',#19052,#15093,#15094);
#15075=DIRECTION('axis',(0.,0.,1.));
#15076=DIRECTION('refdir',(1.,0.,0.));
#15077=DIRECTION('center_axis',(1.,0.,0.));
#15078=DIRECTION('ref_axis',(0.,0.,-1.));
#15079=DIRECTION('center_axis',(-1.,0.,0.));
#15080=DIRECTION('ref_axis',(0.,0.,-1.));
#15081=DIRECTION('',(-1.,0.,0.));
#15082=DIRECTION('center_axis',(-1.,0.,0.));
#15083=DIRECTION('ref_axis',(0.,0.,-1.));
#15084=DIRECTION('center_axis',(1.,0.,0.));
#15085=DIRECTION('ref_axis',(0.,0.,-1.));
#15086=DIRECTION('center_axis',(1.,0.,0.));
#15087=DIRECTION('ref_axis',(0.,0.,-1.));
#15088=DIRECTION('',(-1.,0.,0.));
#15089=DIRECTION('center_axis',(1.,0.,0.));
#15090=DIRECTION('ref_axis',(0.,0.,-1.));
#15091=DIRECTION('center_axis',(1.,0.,0.));
#15092=DIRECTION('ref_axis',(0.,0.,-1.));
#15093=DIRECTION('center_axis',(1.,0.,0.));
#15094=DIRECTION('ref_axis',(0.,0.,-1.));
#19038=CARTESIAN_POINT('',(0.,0.,0.));
#19039=CARTESIAN_POINT('Origin',(2.,11.,4.5));
#19040=CARTESIAN_POINT('',(3.5,11.,5.105));
#19041=CARTESIAN_POINT('Origin',(3.5,11.,4.5));
#19042=CARTESIAN_POINT('',(2.,11.,5.105));
#19043=CARTESIAN_POINT('',(2.,11.,5.105));
#19044=CARTESIAN_POINT('Origin',(2.,11.,4.5));
#19045=CARTESIAN_POINT('Origin',(2.,11.,4.5));
#19046=CARTESIAN_POINT('',(3.5,11.,5.3));
#19047=CARTESIAN_POINT('Origin',(3.5,11.,4.5));
#19048=CARTESIAN_POINT('',(2.,11.,5.3));
#19049=CARTESIAN_POINT('',(2.,11.,5.3));
#19050=CARTESIAN_POINT('Origin',(2.,11.,4.5));
#19051=CARTESIAN_POINT('Origin',(3.5,11.,4.5));
#19052=CARTESIAN_POINT('Origin',(2.,11.,4.5));
#23468=UNCERTAINTY_MEASURE_WITH_UNIT(LENGTH_MEASURE(0.001),#23588,
'DISTANCE_ACCURACY_VALUE',
'Maximum model space distance between geometric entities at asserted c
onnectivities');
#23522=UNCERTAINTY_MEASURE_WITH_UNIT(LENGTH_MEASURE(0.001),#23588,
'DISTANCE_ACCURACY_VALUE',
'Maximum model space distance between geometric entities at asserted c
onnectivities');
#23533=(
GEOMETRIC_REPRESENTATION_CONTEXT(3)
GLOBAL_UNCERTAINTY_ASSIGNED_CONTEXT((#23468))
GLOBAL_UNIT_ASSIGNED_CONTEXT((#23588,#23590,#23591))
REPRESENTATION_CONTEXT('','3D')
);
#23587=(
GEOMETRIC_REPRESENTATION_CONTEXT(3)
GLOBAL_UNCERTAINTY_ASSIGNED_CONTEXT((#23522))
GLOBAL_UNIT_ASSIGNED_CONTEXT((#23588,#23590,#23591))
REPRESENTATION_CONTEXT('','3D')
);
#23588=(
LENGTH_UNIT()
NAMED_UNIT(*)
SI_UNIT(.CENTI.,.METRE.)
);
#23590=(
NAMED_UNIT(*)
PLANE_ANGLE_UNIT()
SI_UNIT($,.RADIAN.)
);
#23591=(
NAMED_UNIT(*)
SI_UNIT($,.STERADIAN.)
SOLID_ANGLE_UNIT()
);
#23602=SHAPE_DEFINITION_REPRESENTATION(#23666,#23835);
#23666=PRODUCT_DEFINITION_SHAPE('',$,#23900);
#23835=SHAPE_REPRESENTATION('',(#13094),#23533);
#23889=PRODUCT_DEFINITION_CONTEXT('part definition',#24083,'design');
#23900=PRODUCT_DEFINITION('Screw bushing','Screw bushing',#23964,#23889);
#23964=PRODUCT_DEFINITION_FORMATION('',$,#24095);
#24083=APPLICATION_CONTEXT(
'Core Data for Automotive Mechanical Design Process');
#24084=PRODUCT_CONTEXT('part definition',#24083,'mechanical');
#24095=PRODUCT('Screw bushing','Screw bushing','Screw bushing',(#24084));
#24212=COLOUR_RGB('Black',0.12,0.14,0.17);
#24213=FILL_AREA_STYLE_COLOUR('',#24212);
#24214=FILL_AREA_STYLE('',(#24213));
#24215=SURFACE_STYLE_FILL_AREA(#24214);
#24216=SURFACE_SIDE_STYLE('',(#24215));
#24217=SURFACE_STYLE_USAGE(.BOTH.,#24216);
#24218=PRESENTATION_STYLE_ASSIGNMENT((#24217));
ENDSEC;
END-ISO-10303-21;
